ISO-10303-21;
HEADER;
/* Generated by software containing ST-Developer
 * from STEP Tools, Inc. (www.steptools.com) 
 */

FILE_DESCRIPTION(
/* description */ (''),
/* implementation_level */ '2;1');

FILE_NAME(
/* name */ 'Motor_Mount.step',
/* time_stamp */ '2026-10-22T16:03:28+06:00',
/* author */ (''),
/* organization */ (''),
/* preprocessor_version */ 'ST-DEVELOPER v20.2',
/* originating_system */ 'Autodesk Translation Framework v15.15.0.0',
/* authorisation */ '');

FILE_SCHEMA (('AUTOMOTIVE_DESIGN { 1 0 10303 214 3 1 1 }'));
ENDSEC;

DATA;
#10=MECHANICAL_DESIGN_GEOMETRIC_PRESENTATION_REPRESENTATION('',(#89),#6096);
#67=SHAPE_REPRESENTATION_RELATIONSHIP('SRR','None',#6142,#78);
#78=ADVANCED_BREP_SHAPE_REPRESENTATION('',(#100),#6090);
#89=STYLED_ITEM('',(#6269),#100);
#100=MANIFOLD_SOLID_BREP('Motor_Mount',#3598);
#120=FACE_BOUND('',#601,.T.);
#121=FACE_BOUND('',#605,.T.);
#122=FACE_BOUND('',#607,.T.);
#123=FACE_BOUND('',#610,.T.);
#232=PLANE('',#3889);
#233=PLANE('',#3890);
#234=PLANE('',#3891);
#235=PLANE('',#3892);
#236=PLANE('',#3893);
#237=PLANE('',#3894);
#238=PLANE('',#3895);
#239=PLANE('',#3896);
#240=PLANE('',#3897);
#241=PLANE('',#3898);
#242=PLANE('',#3899);
#243=PLANE('',#3900);
#244=PLANE('',#3901);
#245=PLANE('',#3902);
#395=FACE_OUTER_BOUND('',#597,.T.);
#396=FACE_OUTER_BOUND('',#598,.T.);
#397=FACE_OUTER_BOUND('',#599,.T.);
#398=FACE_OUTER_BOUND('',#600,.T.);
#399=FACE_OUTER_BOUND('',#602,.T.);
#400=FACE_OUTER_BOUND('',#603,.T.);
#401=FACE_OUTER_BOUND('',#604,.T.);
#402=FACE_OUTER_BOUND('',#606,.T.);
#403=FACE_OUTER_BOUND('',#608,.T.);
#404=FACE_OUTER_BOUND('',#609,.T.);
#405=FACE_OUTER_BOUND('',#611,.T.);
#406=FACE_OUTER_BOUND('',#612,.T.);
#407=FACE_OUTER_BOUND('',#613,.T.);
#408=FACE_OUTER_BOUND('',#614,.T.);
#409=FACE_OUTER_BOUND('',#615,.T.);
#597=EDGE_LOOP('',(#2912,#2913,#2914,#2915));
#598=EDGE_LOOP('',(#2916,#2917,#2918,#2919));
#599=EDGE_LOOP('',(#2920,#2921,#2922,#2923));
#600=EDGE_LOOP('',(#2924,#2925,#2926,#2927));
#601=EDGE_LOOP('',(#2928));
#602=EDGE_LOOP('',(#2929,#2930,#2931,#2932));
#603=EDGE_LOOP('',(#2933,#2934,#2935,#2936));
#604=EDGE_LOOP('',(#2937,#2938,#2939,#2940));
#605=EDGE_LOOP('',(#2941,#2942,#2943,#2944));
#606=EDGE_LOOP('',(#2945,#2946,#2947,#2948,#2949,#2950,#2951,#2952));
#607=EDGE_LOOP('',(#2953));
#608=EDGE_LOOP('',(#2954,#2955,#2956,#2957));
#609=EDGE_LOOP('',(#2958,#2959,#2960,#2961));
#610=EDGE_LOOP('',(#2962,#2963,#2964,#2965));
#611=EDGE_LOOP('',(#2966,#2967,#2968,#2969));
#612=EDGE_LOOP('',(#2970,#2971,#2972,#2973));
#613=EDGE_LOOP('',(#2974,#2975,#2976,#2977));
#614=EDGE_LOOP('',(#2978,#2979,#2980,#2981));
#615=EDGE_LOOP('',(#2982,#2983,#2984,#2985,#2986,#2987,#2988,#2989));
#929=LINE('',#5593,#1308);
#930=LINE('',#5598,#1309);
#931=LINE('',#5600,#1310);
#932=LINE('',#5602,#1311);
#933=LINE('',#5603,#1312);
#934=LINE('',#5606,#1313);
#935=LINE('',#5608,#1314);
#936=LINE('',#5609,#1315);
#937=LINE('',#5612,#1316);
#938=LINE('',#5614,#1317);
#939=LINE('',#5615,#1318);
#940=LINE('',#5617,#1319);
#941=LINE('',#5618,#1320);
#942=LINE('',#5622,#1321);
#943=LINE('',#5624,#1322);
#944=LINE('',#5626,#1323);
#945=LINE('',#5627,#1324);
#946=LINE('',#5630,#1325);
#947=LINE('',#5632,#1326);
#948=LINE('',#5633,#1327);
#949=LINE('',#5636,#1328);
#950=LINE('',#5638,#1329);
#951=LINE('',#5640,#1330);
#952=LINE('',#5642,#1331);
#953=LINE('',#5644,#1332);
#954=LINE('',#5645,#1333);
#955=LINE('',#5649,#1334);
#956=LINE('',#5650,#1335);
#957=LINE('',#5651,#1336);
#958=LINE('',#5654,#1337);
#959=LINE('',#5655,#1338);
#960=LINE('',#5658,#1339);
#961=LINE('',#5659,#1340);
#962=LINE('',#5662,#1341);
#963=LINE('',#5663,#1342);
#964=LINE('',#5665,#1343);
#965=LINE('',#5667,#1344);
#1308=VECTOR('',#4570,11.);
#1309=VECTOR('',#4575,10.);
#1310=VECTOR('',#4576,10.);
#1311=VECTOR('',#4577,10.);
#1312=VECTOR('',#4578,10.);
#1313=VECTOR('',#4581,10.);
#1314=VECTOR('',#4582,10.);
#1315=VECTOR('',#4583,10.);
#1316=VECTOR('',#4586,10.);
#1317=VECTOR('',#4587,10.);
#1318=VECTOR('',#4588,10.);
#1319=VECTOR('',#4591,10.);
#1320=VECTOR('',#4592,10.);
#1321=VECTOR('',#4595,10.);
#1322=VECTOR('',#4596,10.);
#1323=VECTOR('',#4597,10.);
#1324=VECTOR('',#4598,10.);
#1325=VECTOR('',#4601,10.);
#1326=VECTOR('',#4602,10.);
#1327=VECTOR('',#4603,10.);
#1328=VECTOR('',#4606,10.);
#1329=VECTOR('',#4607,10.);
#1330=VECTOR('',#4608,10.);
#1331=VECTOR('',#4609,10.);
#1332=VECTOR('',#4610,10.);
#1333=VECTOR('',#4611,10.);
#1334=VECTOR('',#4614,10.);
#1335=VECTOR('',#4615,10.);
#1336=VECTOR('',#4616,10.);
#1337=VECTOR('',#4619,10.);
#1338=VECTOR('',#4620,10.);
#1339=VECTOR('',#4623,10.);
#1340=VECTOR('',#4624,10.);
#1341=VECTOR('',#4627,10.);
#1342=VECTOR('',#4628,10.);
#1343=VECTOR('',#4631,10.);
#1344=VECTOR('',#4634,10.);
#1540=CIRCLE('',#3887,11.);
#1541=CIRCLE('',#3888,11.);
#1760=VERTEX_POINT('',#5590);
#1761=VERTEX_POINT('',#5592);
#1762=VERTEX_POINT('',#5596);
#1763=VERTEX_POINT('',#5597);
#1764=VERTEX_POINT('',#5599);
#1765=VERTEX_POINT('',#5601);
#1766=VERTEX_POINT('',#5605);
#1767=VERTEX_POINT('',#5607);
#1768=VERTEX_POINT('',#5611);
#1769=VERTEX_POINT('',#5613);
#1770=VERTEX_POINT('',#5620);
#1771=VERTEX_POINT('',#5621);
#1772=VERTEX_POINT('',#5623);
#1773=VERTEX_POINT('',#5625);
#1774=VERTEX_POINT('',#5629);
#1775=VERTEX_POINT('',#5631);
#1776=VERTEX_POINT('',#5635);
#1777=VERTEX_POINT('',#5637);
#1778=VERTEX_POINT('',#5639);
#1779=VERTEX_POINT('',#5641);
#1780=VERTEX_POINT('',#5643);
#1781=VERTEX_POINT('',#5647);
#1782=VERTEX_POINT('',#5648);
#1783=VERTEX_POINT('',#5653);
#1784=VERTEX_POINT('',#5657);
#1785=VERTEX_POINT('',#5661);
#2168=EDGE_CURVE('',#1760,#1760,#1540,.T.);
#2169=EDGE_CURVE('',#1760,#1761,#929,.T.);
#2170=EDGE_CURVE('',#1761,#1761,#1541,.T.);
#2171=EDGE_CURVE('',#1762,#1763,#930,.T.);
#2172=EDGE_CURVE('',#1762,#1764,#931,.T.);
#2173=EDGE_CURVE('',#1765,#1764,#932,.T.);
#2174=EDGE_CURVE('',#1763,#1765,#933,.T.);
#2175=EDGE_CURVE('',#1766,#1762,#934,.T.);
#2176=EDGE_CURVE('',#1766,#1767,#935,.T.);
#2177=EDGE_CURVE('',#1764,#1767,#936,.T.);
#2178=EDGE_CURVE('',#1768,#1766,#937,.T.);
#2179=EDGE_CURVE('',#1768,#1769,#938,.T.);
#2180=EDGE_CURVE('',#1767,#1769,#939,.T.);
#2181=EDGE_CURVE('',#1763,#1768,#940,.T.);
#2182=EDGE_CURVE('',#1769,#1765,#941,.T.);
#2183=EDGE_CURVE('',#1770,#1771,#942,.T.);
#2184=EDGE_CURVE('',#1771,#1772,#943,.T.);
#2185=EDGE_CURVE('',#1772,#1773,#944,.T.);
#2186=EDGE_CURVE('',#1773,#1770,#945,.T.);
#2187=EDGE_CURVE('',#1773,#1774,#946,.T.);
#2188=EDGE_CURVE('',#1775,#1774,#947,.T.);
#2189=EDGE_CURVE('',#1770,#1775,#948,.T.);
#2190=EDGE_CURVE('',#1772,#1776,#949,.T.);
#2191=EDGE_CURVE('',#1777,#1776,#950,.T.);
#2192=EDGE_CURVE('',#1777,#1778,#951,.T.);
#2193=EDGE_CURVE('',#1779,#1778,#952,.T.);
#2194=EDGE_CURVE('',#1779,#1780,#953,.T.);
#2195=EDGE_CURVE('',#1774,#1780,#954,.T.);
#2196=EDGE_CURVE('',#1781,#1782,#955,.T.);
#2197=EDGE_CURVE('',#1782,#1777,#956,.T.);
#2198=EDGE_CURVE('',#1776,#1781,#957,.T.);
#2199=EDGE_CURVE('',#1783,#1782,#958,.T.);
#2200=EDGE_CURVE('',#1778,#1783,#959,.T.);
#2201=EDGE_CURVE('',#1783,#1784,#960,.T.);
#2202=EDGE_CURVE('',#1784,#1779,#961,.T.);
#2203=EDGE_CURVE('',#1785,#1775,#962,.T.);
#2204=EDGE_CURVE('',#1780,#1785,#963,.T.);
#2205=EDGE_CURVE('',#1785,#1784,#964,.T.);
#2206=EDGE_CURVE('',#1781,#1771,#965,.T.);
#2912=ORIENTED_EDGE('',*,*,#2168,.F.);
#2913=ORIENTED_EDGE('',*,*,#2169,.T.);
#2914=ORIENTED_EDGE('',*,*,#2170,.F.);
#2915=ORIENTED_EDGE('',*,*,#2169,.F.);
#2916=ORIENTED_EDGE('',*,*,#2171,.F.);
#2917=ORIENTED_EDGE('',*,*,#2172,.T.);
#2918=ORIENTED_EDGE('',*,*,#2173,.F.);
#2919=ORIENTED_EDGE('',*,*,#2174,.F.);
#2920=ORIENTED_EDGE('',*,*,#2175,.F.);
#2921=ORIENTED_EDGE('',*,*,#2176,.T.);
#2922=ORIENTED_EDGE('',*,*,#2177,.F.);
#2923=ORIENTED_EDGE('',*,*,#2172,.F.);
#2924=ORIENTED_EDGE('',*,*,#2178,.F.);
#2925=ORIENTED_EDGE('',*,*,#2179,.T.);
#2926=ORIENTED_EDGE('',*,*,#2180,.F.);
#2927=ORIENTED_EDGE('',*,*,#2176,.F.);
#2928=ORIENTED_EDGE('',*,*,#2168,.T.);
#2929=ORIENTED_EDGE('',*,*,#2181,.F.);
#2930=ORIENTED_EDGE('',*,*,#2174,.T.);
#2931=ORIENTED_EDGE('',*,*,#2182,.F.);
#2932=ORIENTED_EDGE('',*,*,#2179,.F.);
#2933=ORIENTED_EDGE('',*,*,#2183,.T.);
#2934=ORIENTED_EDGE('',*,*,#2184,.T.);
#2935=ORIENTED_EDGE('',*,*,#2185,.T.);
#2936=ORIENTED_EDGE('',*,*,#2186,.T.);
#2937=ORIENTED_EDGE('',*,*,#2186,.F.);
#2938=ORIENTED_EDGE('',*,*,#2187,.T.);
#2939=ORIENTED_EDGE('',*,*,#2188,.F.);
#2940=ORIENTED_EDGE('',*,*,#2189,.F.);
#2941=ORIENTED_EDGE('',*,*,#2173,.T.);
#2942=ORIENTED_EDGE('',*,*,#2177,.T.);
#2943=ORIENTED_EDGE('',*,*,#2180,.T.);
#2944=ORIENTED_EDGE('',*,*,#2182,.T.);
#2945=ORIENTED_EDGE('',*,*,#2185,.F.);
#2946=ORIENTED_EDGE('',*,*,#2190,.T.);
#2947=ORIENTED_EDGE('',*,*,#2191,.F.);
#2948=ORIENTED_EDGE('',*,*,#2192,.T.);
#2949=ORIENTED_EDGE('',*,*,#2193,.F.);
#2950=ORIENTED_EDGE('',*,*,#2194,.T.);
#2951=ORIENTED_EDGE('',*,*,#2195,.F.);
#2952=ORIENTED_EDGE('',*,*,#2187,.F.);
#2953=ORIENTED_EDGE('',*,*,#2170,.T.);
#2954=ORIENTED_EDGE('',*,*,#2196,.T.);
#2955=ORIENTED_EDGE('',*,*,#2197,.T.);
#2956=ORIENTED_EDGE('',*,*,#2191,.T.);
#2957=ORIENTED_EDGE('',*,*,#2198,.T.);
#2958=ORIENTED_EDGE('',*,*,#2197,.F.);
#2959=ORIENTED_EDGE('',*,*,#2199,.F.);
#2960=ORIENTED_EDGE('',*,*,#2200,.F.);
#2961=ORIENTED_EDGE('',*,*,#2192,.F.);
#2962=ORIENTED_EDGE('',*,*,#2171,.T.);
#2963=ORIENTED_EDGE('',*,*,#2181,.T.);
#2964=ORIENTED_EDGE('',*,*,#2178,.T.);
#2965=ORIENTED_EDGE('',*,*,#2175,.T.);
#2966=ORIENTED_EDGE('',*,*,#2201,.T.);
#2967=ORIENTED_EDGE('',*,*,#2202,.T.);
#2968=ORIENTED_EDGE('',*,*,#2193,.T.);
#2969=ORIENTED_EDGE('',*,*,#2200,.T.);
#2970=ORIENTED_EDGE('',*,*,#2203,.T.);
#2971=ORIENTED_EDGE('',*,*,#2188,.T.);
#2972=ORIENTED_EDGE('',*,*,#2195,.T.);
#2973=ORIENTED_EDGE('',*,*,#2204,.T.);
#2974=ORIENTED_EDGE('',*,*,#2202,.F.);
#2975=ORIENTED_EDGE('',*,*,#2205,.F.);
#2976=ORIENTED_EDGE('',*,*,#2204,.F.);
#2977=ORIENTED_EDGE('',*,*,#2194,.F.);
#2978=ORIENTED_EDGE('',*,*,#2184,.F.);
#2979=ORIENTED_EDGE('',*,*,#2206,.F.);
#2980=ORIENTED_EDGE('',*,*,#2198,.F.);
#2981=ORIENTED_EDGE('',*,*,#2190,.F.);
#2982=ORIENTED_EDGE('',*,*,#2183,.F.);
#2983=ORIENTED_EDGE('',*,*,#2189,.T.);
#2984=ORIENTED_EDGE('',*,*,#2203,.F.);
#2985=ORIENTED_EDGE('',*,*,#2205,.T.);
#2986=ORIENTED_EDGE('',*,*,#2201,.F.);
#2987=ORIENTED_EDGE('',*,*,#2199,.T.);
#2988=ORIENTED_EDGE('',*,*,#2196,.F.);
#2989=ORIENTED_EDGE('',*,*,#2206,.T.);
#3385=CYLINDRICAL_SURFACE('',#3886,11.);
#3502=ADVANCED_FACE('',(#395),#3385,.F.);
#3503=ADVANCED_FACE('',(#396),#232,.F.);
#3504=ADVANCED_FACE('',(#397),#233,.F.);
#3505=ADVANCED_FACE('',(#398,#120),#234,.F.);
#3506=ADVANCED_FACE('',(#399),#235,.F.);
#3507=ADVANCED_FACE('',(#400),#236,.T.);
#3508=ADVANCED_FACE('',(#401,#121),#237,.T.);
#3509=ADVANCED_FACE('',(#402,#122),#238,.F.);
#3510=ADVANCED_FACE('',(#403),#239,.T.);
#3511=ADVANCED_FACE('',(#404,#123),#240,.T.);
#3512=ADVANCED_FACE('',(#405),#241,.T.);
#3513=ADVANCED_FACE('',(#406),#242,.T.);
#3514=ADVANCED_FACE('',(#407),#243,.T.);
#3515=ADVANCED_FACE('',(#408),#244,.T.);
#3516=ADVANCED_FACE('',(#409),#245,.T.);
#3598=CLOSED_SHELL('',(#3502,#3503,#3504,#3505,#3506,#3507,#3508,#3509,
#3510,#3511,#3512,#3513,#3514,#3515,#3516));
#3885=AXIS2_PLACEMENT_3D('',#5588,#4564,#4565);
#3886=AXIS2_PLACEMENT_3D('',#5589,#4566,#4567);
#3887=AXIS2_PLACEMENT_3D('',#5591,#4568,#4569);
#3888=AXIS2_PLACEMENT_3D('',#5594,#4571,#4572);
#3889=AXIS2_PLACEMENT_3D('',#5595,#4573,#4574);
#3890=AXIS2_PLACEMENT_3D('',#5604,#4579,#4580);
#3891=AXIS2_PLACEMENT_3D('',#5610,#4584,#4585);
#3892=AXIS2_PLACEMENT_3D('',#5616,#4589,#4590);
#3893=AXIS2_PLACEMENT_3D('',#5619,#4593,#4594);
#3894=AXIS2_PLACEMENT_3D('',#5628,#4599,#4600);
#3895=AXIS2_PLACEMENT_3D('',#5634,#4604,#4605);
#3896=AXIS2_PLACEMENT_3D('',#5646,#4612,#4613);
#3897=AXIS2_PLACEMENT_3D('',#5652,#4617,#4618);
#3898=AXIS2_PLACEMENT_3D('',#5656,#4621,#4622);
#3899=AXIS2_PLACEMENT_3D('',#5660,#4625,#4626);
#3900=AXIS2_PLACEMENT_3D('',#5664,#4629,#4630);
#3901=AXIS2_PLACEMENT_3D('',#5666,#4632,#4633);
#3902=AXIS2_PLACEMENT_3D('',#5668,#4635,#4636);
#4564=DIRECTION('axis',(0.,0.,1.));
#4565=DIRECTION('refdir',(1.,0.,0.));
#4566=DIRECTION('center_axis',(0.,-1.,0.));
#4567=DIRECTION('ref_axis',(-1.,0.,0.));
#4568=DIRECTION('center_axis',(0.,-1.,0.));
#4569=DIRECTION('ref_axis',(-1.,0.,0.));
#4570=DIRECTION('',(0.,-1.,0.));
#4571=DIRECTION('center_axis',(0.,1.,0.));
#4572=DIRECTION('ref_axis',(-1.,0.,0.));
#4573=DIRECTION('center_axis',(0.,1.,0.));
#4574=DIRECTION('ref_axis',(1.,0.,0.));
#4575=DIRECTION('',(1.,0.,0.));
#4576=DIRECTION('',(0.,0.,-1.));
#4577=DIRECTION('',(-1.,0.,0.));
#4578=DIRECTION('',(0.,0.,-1.));
#4579=DIRECTION('center_axis',(-1.,7.40148683083438E-17,0.));
#4580=DIRECTION('ref_axis',(7.40148683083438E-17,1.,0.));
#4581=DIRECTION('',(7.40148683083438E-17,1.,0.));
#4582=DIRECTION('',(0.,0.,-1.));
#4583=DIRECTION('',(-7.40148683083438E-17,-1.,0.));
#4584=DIRECTION('center_axis',(0.,-1.,0.));
#4585=DIRECTION('ref_axis',(-1.,0.,0.));
#4586=DIRECTION('',(-1.,0.,0.));
#4587=DIRECTION('',(0.,0.,-1.));
#4588=DIRECTION('',(1.,0.,0.));
#4589=DIRECTION('center_axis',(1.,7.40148683083438E-17,0.));
#4590=DIRECTION('ref_axis',(7.40148683083438E-17,-1.,0.));
#4591=DIRECTION('',(7.40148683083438E-17,-1.,0.));
#4592=DIRECTION('',(-7.40148683083438E-17,1.,0.));
#4593=DIRECTION('center_axis',(0.707106781186548,0.,-0.707106781186548));
#4594=DIRECTION('ref_axis',(-0.707106781186548,0.,-0.707106781186548));
#4595=DIRECTION('',(0.707106781186548,0.,0.707106781186548));
#4596=DIRECTION('',(0.,-1.,0.));
#4597=DIRECTION('',(-0.707106781186548,0.,-0.707106781186548));
#4598=DIRECTION('',(0.,1.,0.));
#4599=DIRECTION('center_axis',(0.,0.,-1.));
#4600=DIRECTION('ref_axis',(-1.,0.,0.));
#4601=DIRECTION('',(-1.,0.,0.));
#4602=DIRECTION('',(0.,-1.,0.));
#4603=DIRECTION('',(-1.,0.,0.));
#4604=DIRECTION('center_axis',(0.,1.,0.));
#4605=DIRECTION('ref_axis',(-1.,0.,0.));
#4606=DIRECTION('',(0.,0.,1.));
#4607=DIRECTION('',(0.707106781186548,0.,-0.707106781186548));
#4608=DIRECTION('',(-1.,0.,0.));
#4609=DIRECTION('',(0.707106781186548,0.,0.707106781186548));
#4610=DIRECTION('',(0.,0.,-1.));
#4611=DIRECTION('',(-0.707106781186548,0.,0.707106781186548));
#4612=DIRECTION('center_axis',(0.707106781186548,0.,0.707106781186548));
#4613=DIRECTION('ref_axis',(0.707106781186548,0.,-0.707106781186548));
#4614=DIRECTION('',(-0.707106781186548,0.,0.707106781186548));
#4615=DIRECTION('',(0.,-1.,0.));
#4616=DIRECTION('',(0.,1.,0.));
#4617=DIRECTION('center_axis',(0.,0.,1.));
#4618=DIRECTION('ref_axis',(1.,0.,0.));
#4619=DIRECTION('',(1.,0.,0.));
#4620=DIRECTION('',(0.,1.,0.));
#4621=DIRECTION('center_axis',(-0.707106781186548,0.,0.707106781186548));
#4622=DIRECTION('ref_axis',(0.707106781186548,0.,0.707106781186548));
#4623=DIRECTION('',(-0.707106781186548,0.,-0.707106781186548));
#4624=DIRECTION('',(0.,-1.,0.));
#4625=DIRECTION('center_axis',(-0.707106781186548,0.,-0.707106781186548));
#4626=DIRECTION('ref_axis',(-0.707106781186548,0.,0.707106781186548));
#4627=DIRECTION('',(0.707106781186548,0.,-0.707106781186548));
#4628=DIRECTION('',(0.,1.,0.));
#4629=DIRECTION('center_axis',(-1.,0.,0.));
#4630=DIRECTION('ref_axis',(0.,0.,1.));
#4631=DIRECTION('',(0.,0.,1.));
#4632=DIRECTION('center_axis',(1.,0.,0.));
#4633=DIRECTION('ref_axis',(0.,0.,-1.));
#4634=DIRECTION('',(0.,0.,-1.));
#4635=DIRECTION('center_axis',(0.,1.,0.));
#4636=DIRECTION('ref_axis',(0.,0.,1.));
#5588=CARTESIAN_POINT('',(0.,0.,0.));
#5589=CARTESIAN_POINT('Origin',(4.44089209850063E-15,525.425982185852,41.5000000000007));
#5590=CARTESIAN_POINT('',(11.,525.425982185852,41.5000000000007));
#5591=CARTESIAN_POINT('Origin',(4.44089209850063E-15,525.425982185852,41.5000000000007));
#5592=CARTESIAN_POINT('',(11.,505.5,41.5000000000007));
#5593=CARTESIAN_POINT('',(11.,525.425982185852,41.5000000000007));
#5594=CARTESIAN_POINT('Origin',(4.44089209850063E-15,505.5,41.5000000000007));
#5595=CARTESIAN_POINT('Origin',(-37.5,585.425982185852,83.));
#5596=CARTESIAN_POINT('',(-37.5,585.425982185852,83.));
#5597=CARTESIAN_POINT('',(37.5,585.425982185852,83.));
#5598=CARTESIAN_POINT('',(-44.5030804055581,585.425982185852,83.));
#5599=CARTESIAN_POINT('',(-37.5,585.425982185852,0.));
#5600=CARTESIAN_POINT('',(-37.5,585.425982185852,83.));
#5601=CARTESIAN_POINT('',(37.5,585.425982185852,0.));
#5602=CARTESIAN_POINT('',(7.00308040555807,585.425982185852,1.47437617670221E-12));
#5603=CARTESIAN_POINT('',(37.5,585.425982185852,83.));
#5604=CARTESIAN_POINT('Origin',(-37.5,525.425982185852,83.));
#5605=CARTESIAN_POINT('',(-37.5,525.425982185852,83.));
#5606=CARTESIAN_POINT('',(-37.5,515.462991092926,83.));
#5607=CARTESIAN_POINT('',(-37.5,525.425982185852,0.));
#5608=CARTESIAN_POINT('',(-37.5,525.425982185852,83.));
#5609=CARTESIAN_POINT('',(-37.5,515.462991092926,1.47437617670221E-12));
#5610=CARTESIAN_POINT('Origin',(37.5,525.425982185852,83.));
#5611=CARTESIAN_POINT('',(37.5,525.425982185852,83.));
#5612=CARTESIAN_POINT('',(-7.00308040555806,525.425982185852,83.));
#5613=CARTESIAN_POINT('',(37.5,525.425982185852,0.));
#5614=CARTESIAN_POINT('',(37.5,525.425982185852,83.));
#5615=CARTESIAN_POINT('',(44.5030804055581,525.425982185852,1.47437617670221E-12));
#5616=CARTESIAN_POINT('Origin',(37.5,585.425982185852,83.));
#5617=CARTESIAN_POINT('',(37.5,545.462991092926,83.));
#5618=CARTESIAN_POINT('',(37.5,545.462991092926,1.47437617670221E-12));
#5619=CARTESIAN_POINT('Origin',(49.0061608111161,505.5,2.50000000000147));
#5620=CARTESIAN_POINT('',(46.5061608111161,600.5,1.47437617670221E-12));
#5621=CARTESIAN_POINT('',(51.5061608111161,600.5,5.00000000000147));
#5622=CARTESIAN_POINT('',(46.5046206083369,600.5,-0.00154020277773892));
#5623=CARTESIAN_POINT('',(51.5061608111161,505.5,5.00000000000147));
#5624=CARTESIAN_POINT('',(51.5061608111161,505.5,5.00000000000147));
#5625=CARTESIAN_POINT('',(46.5061608111161,505.5,1.47437617670221E-12));
#5626=CARTESIAN_POINT('',(46.5046206083369,505.5,-0.00154020277773892));
#5627=CARTESIAN_POINT('',(46.5061608111161,505.5,1.47437617670221E-12));
#5628=CARTESIAN_POINT('Origin',(51.5061608111161,505.5,1.47437617670221E-12));
#5629=CARTESIAN_POINT('',(-46.5061608111161,505.5,1.47437617670221E-12));
#5630=CARTESIAN_POINT('',(90.0000000000013,505.5,1.47437617670221E-12));
#5631=CARTESIAN_POINT('',(-46.5061608111161,600.5,1.47437617670221E-12));
#5632=CARTESIAN_POINT('',(-46.5061608111161,505.5,1.47437617670221E-12));
#5633=CARTESIAN_POINT('',(90.0000000000013,600.5,1.47437617670221E-12));
#5634=CARTESIAN_POINT('Origin',(0.,505.5,41.5000000000007));
#5635=CARTESIAN_POINT('',(51.5061608111161,505.5,78.));
#5636=CARTESIAN_POINT('',(51.5061608111161,505.5,-83.));
#5637=CARTESIAN_POINT('',(46.5061608111161,505.5,83.));
#5638=CARTESIAN_POINT('',(46.5046206083369,505.5,83.0015402027792));
#5639=CARTESIAN_POINT('',(-46.5061608111161,505.5,83.));
#5640=CARTESIAN_POINT('',(51.5061608111161,505.5,83.));
#5641=CARTESIAN_POINT('',(-51.5061608111161,505.5,78.));
#5642=CARTESIAN_POINT('',(-46.5046206083369,505.5,83.0015402027792));
#5643=CARTESIAN_POINT('',(-51.5061608111161,505.5,5.00000000000147));
#5644=CARTESIAN_POINT('',(-51.5061608111161,505.5,83.));
#5645=CARTESIAN_POINT('',(-46.5046206083369,505.5,-0.00154020277773892));
#5646=CARTESIAN_POINT('Origin',(49.0061608111161,505.5,80.5));
#5647=CARTESIAN_POINT('',(51.5061608111161,600.5,78.));
#5648=CARTESIAN_POINT('',(46.5061608111161,600.5,83.));
#5649=CARTESIAN_POINT('',(46.5046206083369,600.5,83.0015402027792));
#5650=CARTESIAN_POINT('',(46.5061608111161,505.5,83.));
#5651=CARTESIAN_POINT('',(51.5061608111161,505.5,78.));
#5652=CARTESIAN_POINT('Origin',(-51.5061608111161,505.5,83.));
#5653=CARTESIAN_POINT('',(-46.5061608111161,600.5,83.));
#5654=CARTESIAN_POINT('',(51.5061608111161,600.5,83.));
#5655=CARTESIAN_POINT('',(-46.5061608111161,505.5,83.));
#5656=CARTESIAN_POINT('Origin',(-49.0061608111161,505.5,80.5));
#5657=CARTESIAN_POINT('',(-51.5061608111161,600.5,78.));
#5658=CARTESIAN_POINT('',(-46.5046206083369,600.5,83.0015402027792));
#5659=CARTESIAN_POINT('',(-51.5061608111161,505.5,78.));
#5660=CARTESIAN_POINT('Origin',(-49.0061608111161,505.5,2.50000000000147));
#5661=CARTESIAN_POINT('',(-51.5061608111161,600.5,5.00000000000147));
#5662=CARTESIAN_POINT('',(-46.5046206083369,600.5,-0.00154020277773892));
#5663=CARTESIAN_POINT('',(-51.5061608111161,505.5,5.00000000000147));
#5664=CARTESIAN_POINT('Origin',(-51.5061608111161,505.5,1.47437617670221E-12));
#5665=CARTESIAN_POINT('',(-51.5061608111161,600.5,83.));
#5666=CARTESIAN_POINT('Origin',(51.5061608111161,505.5,83.));
#5667=CARTESIAN_POINT('',(51.5061608111161,600.5,-83.));
#5668=CARTESIAN_POINT('Origin',(0.,600.5,41.5000000000007));
#6077=UNCERTAINTY_MEASURE_WITH_UNIT(LENGTH_MEASURE(0.01),#6097,
'DISTANCE_ACCURACY_VALUE',
'Maximum model space distance between geometric entities at asserted c
onnectivities');
#6083=UNCERTAINTY_MEASURE_WITH_UNIT(LENGTH_MEASURE(0.01),#6097,
'DISTANCE_ACCURACY_VALUE',
'Maximum model space distance between geometric entities at asserted c
onnectivities');
#6090=(
GEOMETRIC_REPRESENTATION_CONTEXT(3)
GLOBAL_UNCERTAINTY_ASSIGNED_CONTEXT((#6077))
GLOBAL_UNIT_ASSIGNED_CONTEXT((#6097,#6099,#6100))
REPRESENTATION_CONTEXT('','3D')
);
#6096=(
GEOMETRIC_REPRESENTATION_CONTEXT(3)
GLOBAL_UNCERTAINTY_ASSIGNED_CONTEXT((#6083))
GLOBAL_UNIT_ASSIGNED_CONTEXT((#6097,#6099,#6100))
REPRESENTATION_CONTEXT('','3D')
);
#6097=(
LENGTH_UNIT()
NAMED_UNIT(*)
SI_UNIT(.MILLI.,.METRE.)
);
#6099=(
NAMED_UNIT(*)
PLANE_ANGLE_UNIT()
SI_UNIT($,.RADIAN.)
);
#6100=(
NAMED_UNIT(*)
SI_UNIT($,.STERADIAN.)
SOLID_ANGLE_UNIT()
);
#6107=SHAPE_DEFINITION_REPRESENTATION(#6119,#6142);
#6119=PRODUCT_DEFINITION_SHAPE('',$,#6155);
#6142=SHAPE_REPRESENTATION('',(#3885),#6090);
#6148=PRODUCT_DEFINITION_CONTEXT('part definition',#6186,'design');
#6155=PRODUCT_DEFINITION('Motor_Mount','Motor_Mount',#6167,#6148);
#6167=PRODUCT_DEFINITION_FORMATION('',$,#6194);
#6186=APPLICATION_CONTEXT(
'Core Data for Automotive Mechanical Design Process');
#6187=PRODUCT_CONTEXT('part definition',#6186,'mechanical');
#6194=PRODUCT('Motor_Mount','Motor_Mount',$,(#6187));
#6263=COLOUR_RGB('Off White',0.89,0.88,0.83);
#6264=FILL_AREA_STYLE_COLOUR('',#6263);
#6265=FILL_AREA_STYLE('',(#6264));
#6266=SURFACE_STYLE_FILL_AREA(#6265);
#6267=SURFACE_SIDE_STYLE('',(#6266));
#6268=SURFACE_STYLE_USAGE(.BOTH.,#6267);
#6269=PRESENTATION_STYLE_ASSIGNMENT((#6268));
ENDSEC;
END-ISO-10303-21;
